ISO-10303-21;
HEADER;
FILE_DESCRIPTION (('STEP AP214'),
    '1' );
FILE_NAME ('Base.step',
    '2026-10-21T18:31:44',
    ( '' ),
    ( '' ),
    'SwSTEP 2.0',
    'SolidWorks 2025',
    '' );
FILE_SCHEMA (( 'AUTOMOTIVE_DESIGN' ));
ENDSEC;

DATA;
#10=CARTESIAN_POINT ( 'NONE',  ( -27.07453251570901642, -8.000000000000003553, -22.50000000000000355 ) ) ;
#48=PRODUCT_DEFINITION ( 'UNKNOWN', '', #15519, #4010 ) ;
#68=DIRECTION ( 'NONE',  ( 0.000000000000000000, 0.000000000000000000, 1.000000000000000000 ) ) ;
#71=CIRCLE ( 'NONE', #15856, 9.000000000000000000 ) ;
#112=DIRECTION ( 'NONE',  ( -0.000000000000000000, -1.000000000000000000, -0.000000000000000000 ) ) ;
#155=CARTESIAN_POINT ( 'NONE',  ( 0.000000000000000000, 73.00000000000001421, 0.000000000000000000 ) ) ;
#159=DIRECTION ( 'NONE',  ( 1.000000000000000000, 0.000000000000000000, 0.000000000000000000 ) ) ;
#186=CARTESIAN_POINT ( 'NONE',  ( 0.000000000000000000, 0.000000000000000000, 0.000000000000000000 ) ) ;
#191=DIRECTION ( 'NONE',  ( -0.000000000000000000, -1.000000000000000000, -0.000000000000000000 ) ) ;
#197=ORIENTED_EDGE ( 'NONE', *, *, #1177, .T. ) ;
#246=CARTESIAN_POINT ( 'NONE',  ( 7.500000000000001776, -24.45288220904212295, 8.693347190813737413 ) ) ;
#248=FACE_OUTER_BOUND ( 'NONE', #11679, .T. ) ;
#255=AXIS2_PLACEMENT_3D ( 'NONE', #5203, #1206, #13232 ) ;
#273=CARTESIAN_POINT ( 'NONE',  ( 12.50000000000000000, -18.00000000000000355, -2.204364238465235822E-15 ) ) ;
#319=EDGE_CURVE ( 'NONE', #9628, #17318, #5798, .T. ) ;
#346=DIRECTION ( 'NONE',  ( 0.000000000000000000, -1.000000000000000000, 0.000000000000000000 ) ) ;
#417=CARTESIAN_POINT ( 'NONE',  ( 7.500000000000002665, -26.57032277106731755, -6.479247348114214766 ) ) ;
#455=ADVANCED_FACE ( 'NONE', ( #248 ), #1382, .T. ) ;
#489=DIRECTION ( 'NONE',  ( 0.000000000000000000, 1.000000000000000000, 0.000000000000000000 ) ) ;
#500=DIRECTION ( 'NONE',  ( 1.000000000000000000, 8.673617379884039170E-17, -0.000000000000000000 ) ) ;
#549=CYLINDRICAL_SURFACE ( 'NONE', #615, 5.000000000000000000 ) ;
#606=CARTESIAN_POINT ( 'NONE',  ( 0.000000000000000000, -8.000000000000000000, 0.000000000000000000 ) ) ;
#607=DIRECTION ( 'NONE',  ( 0.000000000000000000, -1.000000000000000000, 0.000000000000000000 ) ) ;
#615=AXIS2_PLACEMENT_3D ( 'NONE', #2922, #15204, #14943 ) ;
#628=ORIENTED_EDGE ( 'NONE', *, *, #10569, .F. ) ;
#699=DIRECTION ( 'NONE',  ( 9.637352644315592778E-17, -1.000000000000000000, 0.000000000000000000 ) ) ;
#721=EDGE_CURVE ( 'NONE', #1252, #8781, #12071, .T. ) ;
#728=AXIS2_PLACEMENT_3D ( 'NONE', #13183, #2289, #13009 ) ;
#757=EDGE_LOOP ( 'NONE', ( #6516, #2368, #5539, #17381, #12216, #2672, #8645, #13726 ) ) ;
#832=CARTESIAN_POINT ( 'NONE',  ( -7.499999999999996447, -18.00000000000000355, 8.999999999999998224 ) ) ;
#861=DIRECTION ( 'NONE',  ( 0.000000000000000000, 0.000000000000000000, -1.000000000000000000 ) ) ;
#868=( NAMED_UNIT ( * ) SI_UNIT ( $, .STERADIAN. ) SOLID_ANGLE_UNIT ( ) );
#918=CARTESIAN_POINT ( 'NONE',  ( 12.50000000000000000, -18.00000000000000355, -2.204364238465235822E-15 ) ) ;
#941=DIRECTION ( 'NONE',  ( 0.000000000000000000, 1.000000000000000000, 0.000000000000000000 ) ) ;
#953=FACE_OUTER_BOUND ( 'NONE', #2430, .T. ) ;
#967=VERTEX_POINT ( 'NONE', #7344 ) ;
#970=ORIENTED_EDGE ( 'NONE', *, *, #15747, .T. ) ;
#986=EDGE_CURVE ( 'NONE', #11811, #7222, #9746, .T. ) ;
#992=ORIENTED_EDGE ( 'NONE', *, *, #16917, .F. ) ;
#1018=CARTESIAN_POINT ( 'NONE',  ( -7.499999999999998224, -8.000000000000000000, -22.50000000000000355 ) ) ;
#1084=ORIENTED_EDGE ( 'NONE', *, *, #10622, .T. ) ;
#1108=CARTESIAN_POINT ( 'NONE',  ( -7.499999999999995559, -27.00941661075429323, 5.548846425319426956 ) ) ;
#1125=CARTESIAN_POINT ( 'NONE',  ( 0.000000000000000000, 73.00000000000001421, 0.000000000000000000 ) ) ;
#1177=EDGE_CURVE ( 'NONE', #17275, #8372, #10142, .T. ) ;
#1194=AXIS2_PLACEMENT_3D ( 'NONE', #10, #4075, #8337 ) ;
#1206=DIRECTION ( 'NONE',  ( 1.000000000000000000, 8.673617379884039170E-17, -0.000000000000000000 ) ) ;
#1252=VERTEX_POINT ( 'NONE', #3584 ) ;
#1272=ORIENTED_EDGE ( 'NONE', *, *, #2727, .F. ) ;
#1310=DIRECTION ( 'NONE',  ( -1.000000000000000000, -0.000000000000000000, -0.000000000000000000 ) ) ;
#1361=CARTESIAN_POINT ( 'NONE',  ( -7.499999999999997335, -24.46203974633109368, 8.709571264514707423 ) ) ;
#1382=CYLINDRICAL_SURFACE ( 'NONE', #8332, 9.000000000000000000 ) ;
#1386=AXIS2_PLACEMENT_3D ( 'NONE', #9999, #15171, #10961 ) ;
#1405=CARTESIAN_POINT ( 'NONE',  ( 0.000000000000000000, 3.000000000000000000, 0.000000000000000000 ) ) ;
#1420=PLANE ( 'NONE',  #7136 ) ;
#1452=CARTESIAN_POINT ( 'NONE',  ( -7.499999999999995559, -27.79702113870391145, 1.010069558262734590 ) ) ;
#1505=DIRECTION ( 'NONE',  ( 0.000000000000000000, 0.000000000000000000, -1.000000000000000000 ) ) ;
#1556=CARTESIAN_POINT ( 'NONE',  ( 7.500000000000002665, -25.82163707610023096, 7.534909587719538671 ) ) ;
#1585=CARTESIAN_POINT ( 'NONE',  ( 7.500000000000000000, -28.00000000000000000, -9.367496997597600128 ) ) ;
#1587=EDGE_CURVE ( 'NONE', #17275, #11330, #7247, .T. ) ;
#1598=ORIENTED_EDGE ( 'NONE', *, *, #15747, .F. ) ;
#1600=DIRECTION ( 'NONE',  ( 0.000000000000000000, -1.000000000000000000, 0.000000000000000000 ) ) ;
#1601=DIRECTION ( 'NONE',  ( 0.000000000000000000, 0.000000000000000000, -1.000000000000000000 ) ) ;
#1603=ORIENTED_EDGE ( 'NONE', *, *, #15057, .F. ) ;
#1710=ORIENTED_EDGE ( 'NONE', *, *, #6259, .F. ) ;
#1772=VERTEX_POINT ( 'NONE', #11050 ) ;
#1806=ORIENTED_EDGE ( 'NONE', *, *, #1955, .T. ) ;
#1814=CARTESIAN_POINT ( 'NONE',  ( 7.500000000000001776, -23.99662210092440517, 8.932545650451684693 ) ) ;
#1835=ADVANCED_BREP_SHAPE_REPRESENTATION ( '', ( #3043, #16654 ), #13005 ) ;
#1894=LINE ( 'NONE', #7401, #7541 ) ;
#1899=CARTESIAN_POINT ( 'NONE',  ( -7.499999999999996447, -18.00000000000000355, -9.000000000000001776 ) ) ;
#1926=DIRECTION ( 'NONE',  ( 0.000000000000000000, 0.000000000000000000, 1.000000000000000000 ) ) ;
#1932=DIRECTION ( 'NONE',  ( 0.000000000000000000, 0.000000000000000000, 1.000000000000000000 ) ) ;
#1955=EDGE_CURVE ( 'NONE', #17318, #16659, #12956, .T. ) ;
#1964=ORIENTED_EDGE ( 'NONE', *, *, #2233, .T. ) ;
#1977=DIRECTION ( 'NONE',  ( -1.000000000000000000, -0.000000000000000000, -0.000000000000000000 ) ) ;
#2014=EDGE_CURVE ( 'NONE', #16449, #7842, #11636, .T. ) ;
#2102=DIRECTION ( 'NONE',  ( 0.000000000000000000, -1.000000000000000000, 0.000000000000000000 ) ) ;
#2132=EDGE_LOOP ( 'NONE', ( #10988, #8282 ) ) ;
#2153=ORIENTED_EDGE ( 'NONE', *, *, #15578, .F. ) ;
#2192=ORIENTED_EDGE ( 'NONE', *, *, #2367, .T. ) ;
#2194=EDGE_LOOP ( 'NONE', ( #4958, #7926, #1806, #8990 ) ) ;
#2200=AXIS2_PLACEMENT_3D ( 'NONE', #10850, #17382, #2518 ) ;
#2205=DIRECTION ( 'NONE',  ( 1.000000000000000000, 0.000000000000000000, 0.000000000000000000 ) ) ;
#2221=ORIENTED_EDGE ( 'NONE', *, *, #11736, .F. ) ;
#2233=EDGE_CURVE ( 'NONE', #12977, #5187, #10885, .T. ) ;
#2247=AXIS2_PLACEMENT_3D ( 'NONE', #4204, #489, #11103 ) ;
#2262=CYLINDRICAL_SURFACE ( 'NONE', #13586, 12.00000000000000178 ) ;
#2266=ADVANCED_FACE ( 'NONE', ( #16980, #4882 ), #3722, .F. ) ;
#2289=DIRECTION ( 'NONE',  ( 0.000000000000000000, -1.000000000000000000, 0.000000000000000000 ) ) ;
#2322=CARTESIAN_POINT ( 'NONE',  ( 1.469576158976824144E-15, 0.000000000000000000, -12.00000000000000178 ) ) ;
#2367=EDGE_CURVE ( 'NONE', #1772, #4303, #3544, .T. ) ;
#2368=ORIENTED_EDGE ( 'NONE', *, *, #13434, .T. ) ;
#2386=VERTEX_POINT ( 'NONE', #11688 ) ;
#2414=CARTESIAN_POINT ( 'NONE',  ( -7.499999999999995559, -24.66999453389980346, -8.557281619885989343 ) ) ;
#2426=EDGE_CURVE ( 'NONE', #6499, #967, #11775, .T. ) ;
#2430=EDGE_LOOP ( 'NONE', ( #10834, #17171, #4568, #16470, #13280, #10923, #13875, #2192 ) ) ;
#2461=CARTESIAN_POINT ( 'NONE',  ( 0.000000000000000000, -22.00000000000000000, 0.000000000000000000 ) ) ;
#2487=EDGE_CURVE ( 'NONE', #2386, #16561, #4685, .T. ) ;
#2498=ORIENTED_EDGE ( 'NONE', *, *, #319, .T. ) ;
#2503=CARTESIAN_POINT ( 'NONE',  ( -7.499999999999996447, -23.02360215807748745, -9.261711852864912942 ) ) ;
#2518=DIRECTION ( 'NONE',  ( 0.000000000000000000, 0.000000000000000000, -1.000000000000000000 ) ) ;
#2652=ADVANCED_FACE ( 'NONE', ( #5469 ), #7863, .T. ) ;
#2664=CARTESIAN_POINT ( 'NONE',  ( -7.499999999999993783, -28.00000000000000000, -9.367496997597603681 ) ) ;
#2672=ORIENTED_EDGE ( 'NONE', *, *, #721, .T. ) ;
#2678=CARTESIAN_POINT ( 'NONE',  ( -7.499999999999995559, -27.69291120311264720, 2.544524385544278289 ) ) ;
#2694=MECHANICAL_DESIGN_GEOMETRIC_PRESENTATION_REPRESENTATION('',(#12602),#12880);
#2714=LINE ( 'NONE', #5489, #6668 ) ;
#2727=EDGE_CURVE ( 'NONE', #13554, #8820, #5229, .T. ) ;
#2730=CYLINDRICAL_SURFACE ( 'NONE', #13801, 9.000000000000000000 ) ;
#2753=CIRCLE ( 'NONE', #7303, 4.000000000000000000 ) ;
#2760=ORIENTED_EDGE ( 'NONE', *, *, #3222, .T. ) ;
#2782=ORIENTED_EDGE ( 'NONE', *, *, #7001, .F. ) ;
#2785=CARTESIAN_POINT ( 'NONE',  ( 7.500000000000001776, -22.51612366527185927, 9.346045933502388436 ) ) ;
#2817=CARTESIAN_POINT ( 'NONE',  ( 0.000000000000000000, 0.000000000000000000, -22.50000000000000355 ) ) ;
#2851=ORIENTED_EDGE ( 'NONE', *, *, #2727, .T. ) ;
#2855=EDGE_CURVE ( 'NONE', #5187, #7222, #2714, .T. ) ;
#2868=ORIENTED_EDGE ( 'NONE', *, *, #3222, .F. ) ;
#2912=ORIENTED_EDGE ( 'NONE', *, *, #12292, .F. ) ;
#2922=CARTESIAN_POINT ( 'NONE',  ( 0.000000000000000000, 73.00000000000001421, 0.000000000000000000 ) ) ;
#2959=ORIENTED_EDGE ( 'NONE', *, *, #14702, .T. ) ;
#2962=CARTESIAN_POINT ( 'NONE',  ( 7.500000000000000888, -27.79702113870390789, -1.010069558262736145 ) ) ;
#2981=CARTESIAN_POINT ( 'NONE',  ( 7.347880794884121708E-16, -22.00000000000000000, 6.000000000000001776 ) ) ;
#3041=CARTESIAN_POINT ( 'NONE',  ( -7.499999999999998224, -8.000000000000000000, 9.367496997597587693 ) ) ;
#3043=MANIFOLD_SOLID_BREP ( 'Boss-Extrude4', #10309 ) ;
#3051=DIRECTION ( 'NONE',  ( 0.000000000000000000, 0.000000000000000000, -1.000000000000000000 ) ) ;
#3052=CARTESIAN_POINT ( 'NONE',  ( 7.500000000000003553, -27.54571194363308706, 3.584587286925209337 ) ) ;
#3078=DIRECTION ( 'NONE',  ( 0.000000000000000000, -0.000000000000000000, 1.000000000000000000 ) ) ;
#3080=CIRCLE ( 'NONE', #1386, 12.00000000000000178 ) ;
#3104=CARTESIAN_POINT ( 'NONE',  ( 0.000000000000000000, 3.000000000000000000, 0.000000000000000000 ) ) ;
#3164=AXIS2_PLACEMENT_3D ( 'NONE', #11409, #3521, #1926 ) ;
#3173=AXIS2_PLACEMENT_3D ( 'NONE', #7291, #7642, #10209 ) ;
#3203=CARTESIAN_POINT ( 'NONE',  ( -12.50000000000000000, -18.00000000000000355, -2.204364238465235822E-15 ) ) ;
#3222=EDGE_CURVE ( 'NONE', #8820, #967, #8099, .T. ) ;
#3313=CARTESIAN_POINT ( 'NONE',  ( -12.50000000000000000, -18.00000000000000355, -2.204364238465235822E-15 ) ) ;
#3351=DIRECTION ( 'NONE',  ( -0.000000000000000000, 1.000000000000000000, -0.000000000000000000 ) ) ;
#3380=AXIS2_PLACEMENT_3D ( 'NONE', #4287, #5629, #12153 ) ;
#3427=CYLINDRICAL_SURFACE ( 'NONE', #15772, 22.50000000000000355 ) ;
#3439=CIRCLE ( 'NONE', #9964, 4.000000000000000000 ) ;
#3446=LINE ( 'NONE', #11324, #14177 ) ;
#3448=CIRCLE ( 'NONE', #5155, 12.00000000000000178 ) ;
#3464=VECTOR ( 'NONE', #10530, 1000.000000000000000 ) ;
#3521=DIRECTION ( 'NONE',  ( 0.000000000000000000, 1.000000000000000000, 0.000000000000000000 ) ) ;
#3537=DIRECTION ( 'NONE',  ( 0.000000000000000000, 0.000000000000000000, -1.000000000000000000 ) ) ;
#3544=CIRCLE ( 'NONE', #728, 12.00000000000000178 ) ;
#3584=CARTESIAN_POINT ( 'NONE',  ( 7.500000000000000888, -22.00000000000000000, 9.367496997597600128 ) ) ;
#3585=FACE_OUTER_BOUND ( 'NONE', #16444, .T. ) ;
#3600=EDGE_CURVE ( 'NONE', #8166, #1772, #5243, .T. ) ;
#3663=FACE_OUTER_BOUND ( 'NONE', #13105, .T. ) ;
#3671=ORIENTED_EDGE ( 'NONE', *, *, #14702, .F. ) ;
#3672=DIRECTION ( 'NONE',  ( -1.000000000000000000, -8.862145109134287319E-17, 0.000000000000000000 ) ) ;
#3681=CIRCLE ( 'NONE', #10198, 12.00000000000000178 ) ;
#3722=PLANE ( 'NONE',  #6954 ) ;
#3745=CIRCLE ( 'NONE', #4312, 22.50000000000000355 ) ;
#3767=CARTESIAN_POINT ( 'NONE',  ( -7.499999999999994671, -27.00452558693060467, -5.560661329642323736 ) ) ;
#3785=DIRECTION ( 'NONE',  ( -0.000000000000000000, -0.000000000000000000, 1.000000000000000000 ) ) ;
#3790=SHAPE_DEFINITION_REPRESENTATION ( #6933, #5468 ) ;
#3851=CARTESIAN_POINT ( 'NONE',  ( -7.499999999999995559, -27.55009420329275827, 3.560038493048078845 ) ) ;
#3894=DIRECTION ( 'NONE',  ( -1.000000000000000000, -8.673617379884037937E-17, 0.000000000000000000 ) ) ;
#3906=CIRCLE ( 'NONE', #10419, 12.00000000000000178 ) ;
#3907=ORIENTED_EDGE ( 'NONE', *, *, #15057, .T. ) ;
#3922=CIRCLE ( 'NONE', #8466, 9.000000000000000000 ) ;
#3938=CARTESIAN_POINT ( 'NONE',  ( -7.499999999999993783, -26.56718630404941806, -6.484415072061725738 ) ) ;
#3955=CARTESIAN_POINT ( 'NONE',  ( 12.50000000000000000, -22.00000000000000355, -1.714505518806294835E-15 ) ) ;
#3957=CARTESIAN_POINT ( 'NONE',  ( -12.50000000000000000, -18.00000000000000355, -2.204364238465235822E-15 ) ) ;
#4010=PRODUCT_DEFINITION_CONTEXT ( 'detailed design', #16226, 'design' ) ;
#4028=CIRCLE ( 'NONE', #13066, 6.000000000000001776 ) ;
#4065=FACE_OUTER_BOUND ( 'NONE', #17444, .T. ) ;
#4075=DIRECTION ( 'NONE',  ( -1.772429021826857464E-16, 1.000000000000000000, 0.000000000000000000 ) ) ;
#4088=PRODUCT ( 'Base', 'Base', '', ( #6714 ) ) ;
#4113=CARTESIAN_POINT ( 'NONE',  ( -7.499999999999996447, -27.18121722713999944, 5.064597142177448497 ) ) ;
#4130=CARTESIAN_POINT ( 'NONE',  ( 7.500000000000000888, -22.00000000000000000, 9.367496997597600128 ) ) ;
#4147=DIRECTION ( 'NONE',  ( 1.000000000000000000, 0.000000000000000000, -1.224646799147353207E-16 ) ) ;
#4204=CARTESIAN_POINT ( 'NONE',  ( 0.000000000000000000, 3.000000000000000000, 0.000000000000000000 ) ) ;
#4224=CIRCLE ( 'NONE', #16348, 4.000000000000000000 ) ;
#4254=CARTESIAN_POINT ( 'NONE',  ( 0.000000000000000000, 3.000000000000000000, 0.000000000000000000 ) ) ;
#4276=FACE_OUTER_BOUND ( 'NONE', #5005, .T. ) ;
#4287=CARTESIAN_POINT ( 'NONE',  ( -7.499999999999996447, -18.00000000000000355, -2.204364238465235822E-15 ) ) ;
#4301=ORIENTED_EDGE ( 'NONE', *, *, #17013, .F. ) ;
#4303=VERTEX_POINT ( 'NONE', #2322 ) ;
#4305=DIRECTION ( 'NONE',  ( 1.000000000000000000, 0.000000000000000000, 0.000000000000000000 ) ) ;
#4312=AXIS2_PLACEMENT_3D ( 'NONE', #9606, #14958, #7121 ) ;
#4335=DIRECTION ( 'NONE',  ( 0.000000000000000000, 0.000000000000000000, 1.000000000000000000 ) ) ;
#4349=FACE_OUTER_BOUND ( 'NONE', #9451, .T. ) ;
#4397=CARTESIAN_POINT ( 'NONE',  ( 7.500000000000000888, -21.99999999999990052, -9.367496997597653419 ) ) ;
#4427=AXIS2_PLACEMENT_3D ( 'NONE', #17098, #7489, #3672 ) ;
#4428=LINE ( 'NONE', #1585, #7937 ) ;
#4463=CARTESIAN_POINT ( 'NONE',  ( -7.499999999999996447, -22.00000000000000000, -9.367496997597603681 ) ) ;
#4482=VERTEX_POINT ( 'NONE', #13040 ) ;
#4487=CARTESIAN_POINT ( 'NONE',  ( 7.500000000000001776, -23.27245777243038916, -9.199283337799341709 ) ) ;
#4496=DIRECTION ( 'NONE',  ( -0.000000000000000000, 1.000000000000000000, -0.000000000000000000 ) ) ;
#4568=ORIENTED_EDGE ( 'NONE', *, *, #7589, .T. ) ;
#4576=CARTESIAN_POINT ( 'NONE',  ( 7.500000000000002665, -22.25853674790688075, -9.367496997597603681 ) ) ;
#4607=CARTESIAN_POINT ( 'NONE',  ( 0.000000000000000000, 3.000000000000000000, -5.000000000000000000 ) ) ;
#4653=ORIENTED_EDGE ( 'NONE', *, *, #13992, .F. ) ;
#4663=CARTESIAN_POINT ( 'NONE',  ( 7.500000000000000888, -27.17584396961776250, 5.080312676971243668 ) ) ;
#4685=CIRCLE ( 'NONE', #11458, 12.00000000000000178 ) ;
#4739=APPLICATION_CONTEXT ( 'automotive_design' ) ;
#4749=CARTESIAN_POINT ( 'NONE',  ( -7.499999999999996447, -22.25602869842714071, -9.367496997597605457 ) ) ;
#4768=ORIENTED_EDGE ( 'NONE', *, *, #11319, .T. ) ;
#4772=CARTESIAN_POINT ( 'NONE',  ( 0.000000000000000000, -28.00000000000000000, 0.000000000000000000 ) ) ;
#4774=LINE ( 'NONE', #6113, #11646 ) ;
#4821=CYLINDRICAL_SURFACE ( 'NONE', #7888, 9.000000000000000000 ) ;
#4827=FACE_BOUND ( 'NONE', #15237, .T. ) ;
#4882=FACE_BOUND ( 'NONE', #7533, .T. ) ;
#4900=ORIENTED_EDGE ( 'NONE', *, *, #15702, .T. ) ;
#4958=ORIENTED_EDGE ( 'NONE', *, *, #14546, .F. ) ;
#5005=EDGE_LOOP ( 'NONE', ( #3671, #7208 ) ) ;
#5007=ORIENTED_EDGE ( 'NONE', *, *, #11736, .T. ) ;
#5031=CARTESIAN_POINT ( 'NONE',  ( 0.000000000000000000, -28.00000000000000000, 0.000000000000000000 ) ) ;
#5035=EDGE_CURVE ( 'NONE', #16561, #13897, #6133, .T. ) ;
#5051=VERTEX_POINT ( 'NONE', #4463 ) ;
#5099=ORIENTED_EDGE ( 'NONE', *, *, #5543, .T. ) ;
#5122=CARTESIAN_POINT ( 'NONE',  ( 0.000000000000000000, 3.000000000000000000, 0.000000000000000000 ) ) ;
#5141=ORIENTED_EDGE ( 'NONE', *, *, #8742, .T. ) ;
#5146=VECTOR ( 'NONE', #3785, 1000.000000000000000 ) ;
#5155=AXIS2_PLACEMENT_3D ( 'NONE', #12121, #6741, #1505 ) ;
#5181=AXIS2_PLACEMENT_3D ( 'NONE', #8064, #6911, #13427 ) ;
#5187=VERTEX_POINT ( 'NONE', #12476 ) ;
#5194=CARTESIAN_POINT ( 'NONE',  ( -7.499999999999994671, -22.51433466932076399, 9.346209313438661681 ) ) ;
#5203=CARTESIAN_POINT ( 'NONE',  ( -22.50000000000000355, -18.00000000000000711, -2.204364238465235822E-15 ) ) ;
#5229=LINE ( 'NONE', #15894, #16223 ) ;
#5243=LINE ( 'NONE', #14667, #16251 ) ;
#5283=CARTESIAN_POINT ( 'NONE',  ( -7.499999999999994671, -27.44685421792581081, -4.091673783487177474 ) ) ;
#5300=DIRECTION ( 'NONE',  ( 0.000000000000000000, 0.000000000000000000, 1.000000000000000000 ) ) ;
#5350=DIRECTION ( 'NONE',  ( 0.000000000000000000, -0.000000000000000000, 1.000000000000000000 ) ) ;
#5352=CARTESIAN_POINT ( 'NONE',  ( 0.000000000000000000, -28.00000000000000000, -6.000000000000001776 ) ) ;
#5365=CARTESIAN_POINT ( 'NONE',  ( -7.499999999999995559, -27.45244706754152375, 4.067225351102819353 ) ) ;
#5420=DIRECTION ( 'NONE',  ( 0.000000000000000000, 0.000000000000000000, -1.000000000000000000 ) ) ;
#5455=EDGE_CURVE ( 'NONE', #14868, #9538, #15125, .T. ) ;
#5468=SHAPE_REPRESENTATION ( 'Base', ( #16654 ), #13005 ) ;
#5469=FACE_OUTER_BOUND ( 'NONE', #17121, .T. ) ;
#5489=CARTESIAN_POINT ( 'NONE',  ( 12.50000000000000000, -18.00000000000000355, -9.000000000000001776 ) ) ;
#5539=ORIENTED_EDGE ( 'NONE', *, *, #14268, .T. ) ;
#5543=EDGE_CURVE ( 'NONE', #12977, #11811, #1894, .T. ) ;
#5545=CARTESIAN_POINT ( 'NONE',  ( -7.499999999999995559, -25.08439332921293285, 8.253836299850743075 ) ) ;
#5561=AXIS2_PLACEMENT_3D ( 'NONE', #13978, #5797, #9954 ) ;
#5580=DIRECTION ( 'NONE',  ( 0.000000000000000000, 0.000000000000000000, 1.000000000000000000 ) ) ;
#5621=TOROIDAL_SURFACE ( 'NONE', #13499, 6.000000000000001776, 6.000000000000000000 ) ;
#5629=DIRECTION ( 'NONE',  ( -1.000000000000000000, -1.301042606982605567E-16, -0.000000000000000000 ) ) ;
#5650=CARTESIAN_POINT ( 'NONE',  ( 7.499999999999996447, -8.000000000000000000, -9.367496997597600128 ) ) ;
#5653=CARTESIAN_POINT ( 'NONE',  ( 12.50000000000000000, -18.00000000000000355, -2.204364238465235822E-15 ) ) ;
#5684=DIRECTION ( 'NONE',  ( -1.000000000000000000, -0.000000000000000000, -0.000000000000000000 ) ) ;
#5700=DIRECTION ( 'NONE',  ( 0.000000000000000000, 1.000000000000000000, 0.000000000000000000 ) ) ;
#5708=ADVANCED_FACE ( 'NONE', ( #12782 ), #6167, .F. ) ;
#5734=ORIENTED_EDGE ( 'NONE', *, *, #2233, .F. ) ;
#5737=CARTESIAN_POINT ( 'NONE',  ( 7.500000000000001776, -25.65291190719445780, -7.723695278929457508 ) ) ;
#5754=( NAMED_UNIT ( * ) PLANE_ANGLE_UNIT ( ) SI_UNIT ( $, .RADIAN. ) );
#5775=DIRECTION ( 'NONE',  ( -0.000000000000000000, 1.000000000000000000, -0.000000000000000000 ) ) ;
#5797=DIRECTION ( 'NONE',  ( -1.000000000000000000, -0.000000000000000000, -0.000000000000000000 ) ) ;
#5798=CIRCLE ( 'NONE', #6074, 4.000000000000000000 ) ;
#5808=ADVANCED_FACE ( 'NONE', ( #14091, #4827 ), #6082, .F. ) ;
#5835=CARTESIAN_POINT ( 'NONE',  ( 0.000000000000000000, -22.00000000000000000, 12.00000000000000178 ) ) ;
#5857=CYLINDRICAL_SURFACE ( 'NONE', #6476, 9.000000000000000000 ) ;
#5912=CARTESIAN_POINT ( 'NONE',  ( 7.500000000000001776, -27.73625732136942901, 2.063574628993722015 ) ) ;
#5928=CARTESIAN_POINT ( 'NONE',  ( 0.000000000000000000, 3.000000000000000000, 0.000000000000000000 ) ) ;
#5935=CYLINDRICAL_SURFACE ( 'NONE', #10232, 12.00000000000000178 ) ;
#5938=SHAPE_REPRESENTATION_RELATIONSHIP ( 'NONE' , 'NONE' ,  #5468, #1835 ) ;
#5950=ORIENTED_EDGE ( 'NONE', *, *, #6259, .T. ) ;
#6000=CARTESIAN_POINT ( 'NONE',  ( 7.500000000000000000, -25.08364130939903092, 8.254396200996687583 ) ) ;
#6010=DIRECTION ( 'NONE',  ( 0.000000000000000000, 0.000000000000000000, -1.000000000000000000 ) ) ;
#6021=DIRECTION ( 'NONE',  ( 1.000000000000000000, 8.673617379884037937E-17, 0.000000000000000000 ) ) ;
#6046=ADVANCED_FACE ( 'NONE', ( #7780 ), #6361, .T. ) ;
#6074=AXIS2_PLACEMENT_3D ( 'NONE', #3957, #159, #8039 ) ;
#6082=PLANE ( 'NONE',  #10093 ) ;
#6090=DIRECTION ( 'NONE',  ( 0.000000000000000000, 1.000000000000000000, 0.000000000000000000 ) ) ;
#6113=CARTESIAN_POINT ( 'NONE',  ( 2.755455298081545172E-15, 3.000000000000000000, 22.50000000000000355 ) ) ;
#6133=CIRCLE ( 'NONE', #5561, 6.000000000000000000 ) ;
#6148=CARTESIAN_POINT ( 'NONE',  ( 2.755455298081545172E-15, 3.000000000000000000, 22.50000000000000355 ) ) ;
#6167=PLANE ( 'NONE',  #4427 ) ;
#6203=LINE ( 'NONE', #11589, #16638 ) ;
#6249=EDGE_LOOP ( 'NONE', ( #1964, #5950 ) ) ;
#6259=EDGE_CURVE ( 'NONE', #5187, #12977, #14887, .T. ) ;
#6287=AXIS2_PLACEMENT_3D ( 'NONE', #6511, #8097, #17182 ) ;
#6314=ORIENTED_EDGE ( 'NONE', *, *, #15264, .F. ) ;
#6357=AXIS2_PLACEMENT_3D ( 'NONE', #14371, #6021, #699 ) ;
#6361=CYLINDRICAL_SURFACE ( 'NONE', #8165, 22.50000000000000355 ) ;
#6380=LINE ( 'NONE', #11763, #3464 ) ;
#6383=VERTEX_POINT ( 'NONE', #5650 ) ;
#6386=DIRECTION ( 'NONE',  ( 0.000000000000000000, 0.000000000000000000, -1.000000000000000000 ) ) ;
#6404=ORIENTED_EDGE ( 'NONE', *, *, #10040, .F. ) ;
#6409=ORIENTED_EDGE ( 'NONE', *, *, #5455, .F. ) ;
#6428=DIRECTION ( 'NONE',  ( -1.301042606982605567E-16, 1.000000000000000000, 0.000000000000000000 ) ) ;
#6433=DIRECTION ( 'NONE',  ( -0.000000000000000000, 1.000000000000000000, -0.000000000000000000 ) ) ;
#6445=DIRECTION ( 'NONE',  ( 0.000000000000000000, 0.000000000000000000, -1.000000000000000000 ) ) ;
#6448=EDGE_LOOP ( 'NONE', ( #2153, #13085 ) ) ;
#6449=DIRECTION ( 'NONE',  ( -0.000000000000000000, -1.000000000000000000, -0.000000000000000000 ) ) ;
#6476=AXIS2_PLACEMENT_3D ( 'NONE', #273, #5684, #12731 ) ;
#6499=VERTEX_POINT ( 'NONE', #1899 ) ;
#6511=CARTESIAN_POINT ( 'NONE',  ( 7.500000000000000888, -18.00000000000000355, -2.204364238465235822E-15 ) ) ;
#6516=ORIENTED_EDGE ( 'NONE', *, *, #2487, .T. ) ;
#6524=CARTESIAN_POINT ( 'NONE',  ( -7.499999999999996447, -25.28385182205995463, 8.084116494856628421 ) ) ;
#6567=DIRECTION ( 'NONE',  ( -0.000000000000000000, 1.000000000000000000, -0.000000000000000000 ) ) ;
#6622=DIRECTION ( 'NONE',  ( 0.000000000000000000, 0.000000000000000000, -1.000000000000000000 ) ) ;
#6624=CARTESIAN_POINT ( 'NONE',  ( -7.499999999999998224, -8.000000000000000000, -22.50000000000000355 ) ) ;
#6646=FACE_BOUND ( 'NONE', #12655, .T. ) ;
#6652=ADVANCED_FACE ( 'NONE', ( #13831 ), #13222, .T. ) ;
#6664=ORIENTED_EDGE ( 'NONE', *, *, #12732, .F. ) ;
#6668=VECTOR ( 'NONE', #1310, 1000.000000000000000 ) ;
#6678=CARTESIAN_POINT ( 'NONE',  ( -7.499999999999996447, -18.00000000000000355, -2.204364238465235822E-15 ) ) ;
#6690=CARTESIAN_POINT ( 'NONE',  ( -7.499999999999995559, -27.80914044117234596, -0.5315352956498873294 ) ) ;
#6694=EDGE_CURVE ( 'NONE', #17318, #9628, #2753, .T. ) ;
#6714=PRODUCT_CONTEXT ( 'NONE', #4739, 'mechanical' ) ;
#6741=DIRECTION ( 'NONE',  ( 0.000000000000000000, -1.000000000000000000, 0.000000000000000000 ) ) ;
#6749=ORIENTED_EDGE ( 'NONE', *, *, #6694, .T. ) ;
#6775=AXIS2_PLACEMENT_3D ( 'NONE', #17205, #13314, #941 ) ;
#6779=CARTESIAN_POINT ( 'NONE',  ( -7.499999999999992895, -22.25853674790686298, 9.367496997597607233 ) ) ;
#6821=DIRECTION ( 'NONE',  ( 0.000000000000000000, 1.000000000000000000, 0.000000000000000000 ) ) ;
#6828=DIRECTION ( 'NONE',  ( -1.000000000000000000, -0.000000000000000000, -0.000000000000000000 ) ) ;
#6838=DIRECTION ( 'NONE',  ( 1.000000000000000000, 0.000000000000000000, 0.000000000000000000 ) ) ;
#6864=ORIENTED_EDGE ( 'NONE', *, *, #8742, .F. ) ;
#6870=CARTESIAN_POINT ( 'NONE',  ( -7.499999999999996447, -21.99999999999990052, 9.367496997597656971 ) ) ;
#6911=DIRECTION ( 'NONE',  ( 1.000000000000000000, 0.000000000000000000, 0.000000000000000000 ) ) ;
#6920=FACE_OUTER_BOUND ( 'NONE', #11163, .T. ) ;
#6933=PRODUCT_DEFINITION_SHAPE ( 'NONE', 'NONE',  #48 ) ;
#6954=AXIS2_PLACEMENT_3D ( 'NONE', #15990, #3894, #15637 ) ;
#6968=ORIENTED_EDGE ( 'NONE', *, *, #10040, .T. ) ;
#6975=DIRECTION ( 'NONE',  ( 0.000000000000000000, 0.000000000000000000, 1.000000000000000000 ) ) ;
#6992=DIRECTION ( 'NONE',  ( 0.000000000000000000, 1.000000000000000000, 0.000000000000000000 ) ) ;
#6999=PLANE ( 'NONE',  #5181 ) ;
#7001=EDGE_CURVE ( 'NONE', #4482, #8166, #3906, .T. ) ;
#7048=CARTESIAN_POINT ( 'NONE',  ( 0.000000000000000000, -8.000000000000000000, 0.000000000000000000 ) ) ;
#7061=CARTESIAN_POINT ( 'NONE',  ( 7.500000000000003553, -27.44685421792581792, 4.091673783487185467 ) ) ;
#7121=DIRECTION ( 'NONE',  ( 0.000000000000000000, 0.000000000000000000, 1.000000000000000000 ) ) ;
#7136=AXIS2_PLACEMENT_3D ( 'NONE', #15022, #1600, #9758 ) ;
#7137=ADVANCED_FACE ( 'NONE', ( #11392 ), #5621, .T. ) ;
#7145=CARTESIAN_POINT ( 'NONE',  ( 7.500000000000000888, -27.79580463407382496, 1.043242051446493734 ) ) ;
#7164=CARTESIAN_POINT ( 'NONE',  ( 0.000000000000000000, -28.00000000000000000, 0.000000000000000000 ) ) ;
#7208=ORIENTED_EDGE ( 'NONE', *, *, #12672, .F. ) ;
#7222=VERTEX_POINT ( 'NONE', #7587 ) ;
#7228=CARTESIAN_POINT ( 'NONE',  ( 7.500000000000002665, -27.18121722713998523, -5.064597142177446720 ) ) ;
#7247=LINE ( 'NONE', #13848, #12867 ) ;
#7279=CARTESIAN_POINT ( 'NONE',  ( 6.123233995736766282E-16, 73.00000000000001421, 5.000000000000000000 ) ) ;
#7285=CARTESIAN_POINT ( 'NONE',  ( 1.469576158976824144E-15, -28.00000000000000000, -12.00000000000000178 ) ) ;
#7291=CARTESIAN_POINT ( 'NONE',  ( 0.000000000000000000, 73.00000000000001421, 0.000000000000000000 ) ) ;
#7303=AXIS2_PLACEMENT_3D ( 'NONE', #16403, #4305, #15063 ) ;
#7308=ORIENTED_EDGE ( 'NONE', *, *, #319, .F. ) ;
#7315=VECTOR ( 'NONE', #8095, 1000.000000000000000 ) ;
#7328=AXIS2_PLACEMENT_3D ( 'NONE', #10422, #607, #6445 ) ;
#7344=CARTESIAN_POINT ( 'NONE',  ( -12.50000000000000000, -18.00000000000000355, -9.000000000000001776 ) ) ;
#7355=DIRECTION ( 'NONE',  ( 1.000000000000000000, 8.673617379884039170E-17, -0.000000000000000000 ) ) ;
#7369=CIRCLE ( 'NONE', #2247, 22.50000000000000355 ) ;
#7378=DIRECTION ( 'NONE',  ( 0.000000000000000000, 0.000000000000000000, -1.000000000000000000 ) ) ;
#7388=ORIENTED_EDGE ( 'NONE', *, *, #13084, .F. ) ;
#7401=CARTESIAN_POINT ( 'NONE',  ( 12.50000000000000000, -18.00000000000000355, 8.999999999999998224 ) ) ;
#7436=DIRECTION ( 'NONE',  ( -0.000000000000000000, -1.000000000000000000, -0.000000000000000000 ) ) ;
#7438=ADVANCED_FACE ( 'NONE', ( #11000, #4276 ), #11089, .F. ) ;
#7441=AXIS2_PLACEMENT_3D ( 'NONE', #1405, #6821, #3078 ) ;
#7489=DIRECTION ( 'NONE',  ( -8.862145109134287319E-17, 1.000000000000000000, 0.000000000000000000 ) ) ;
#7515=VECTOR ( 'NONE', #14662, 1000.000000000000000 ) ;
#7533=EDGE_LOOP ( 'NONE', ( #16126, #4653 ) ) ;
#7541=VECTOR ( 'NONE', #1977, 1000.000000000000000 ) ;
#7587=CARTESIAN_POINT ( 'NONE',  ( 7.500000000000000888, -18.00000000000000355, -9.000000000000001776 ) ) ;
#7589=EDGE_CURVE ( 'NONE', #5051, #14868, #14774, .T. ) ;
#7622=ORIENTED_EDGE ( 'NONE', *, *, #721, .F. ) ;
#7642=DIRECTION ( 'NONE',  ( 0.000000000000000000, 1.000000000000000000, 0.000000000000000000 ) ) ;
#7672=DIRECTION ( 'NONE',  ( 0.000000000000000000, -0.000000000000000000, 1.000000000000000000 ) ) ;
#7686=ORIENTED_EDGE ( 'NONE', *, *, #1587, .F. ) ;
#7693=AXIS2_PLACEMENT_3D ( 'NONE', #3104, #5700, #8531 ) ;
#7780=FACE_OUTER_BOUND ( 'NONE', #11027, .T. ) ;
#7822=EDGE_LOOP ( 'NONE', ( #8256, #15020, #5141, #1272 ) ) ;
#7842=VERTEX_POINT ( 'NONE', #2817 ) ;
#7847=CARTESIAN_POINT ( 'NONE',  ( -7.499999999999998224, -25.82389322351430039, 7.532295102519082519 ) ) ;
#7863=CYLINDRICAL_SURFACE ( 'NONE', #13970, 5.000000000000000000 ) ;
#7888=AXIS2_PLACEMENT_3D ( 'NONE', #918, #10222, #15662 ) ;
#7892=DIRECTION ( 'NONE',  ( -3.552713678800500929E-15, 0.000000000000000000, -1.000000000000000000 ) ) ;
#7916=ADVANCED_FACE ( 'NONE', ( #14127 ), #5857, .T. ) ;
#7926=ORIENTED_EDGE ( 'NONE', *, *, #6694, .F. ) ;
#7927=ORIENTED_EDGE ( 'NONE', *, *, #9880, .F. ) ;
#7937=VECTOR ( 'NONE', #8508, 1000.000000000000000 ) ;
#7948=DIRECTION ( 'NONE',  ( -0.000000000000000000, -1.000000000000000000, -0.000000000000000000 ) ) ;
#7985=DIRECTION ( 'NONE',  ( -0.000000000000000000, 1.000000000000000000, -0.000000000000000000 ) ) ;
#8001=CIRCLE ( 'NONE', #9699, 22.50000000000000355 ) ;
#8029=FACE_OUTER_BOUND ( 'NONE', #2194, .T. ) ;
#8039=DIRECTION ( 'NONE',  ( 0.000000000000000000, 0.000000000000000000, -1.000000000000000000 ) ) ;
#8064=CARTESIAN_POINT ( 'NONE',  ( -12.50000000000000000, -18.00000000000000355, -2.204364238465235822E-15 ) ) ;
#8081=CARTESIAN_POINT ( 'NONE',  ( 12.50000000000000000, -18.00000000000000355, -2.204364238465235822E-15 ) ) ;
#8095=DIRECTION ( 'NONE',  ( -0.000000000000000000, 1.000000000000000000, -0.000000000000000000 ) ) ;
#8097=DIRECTION ( 'NONE',  ( 1.000000000000000000, 8.673617379884037937E-17, 0.000000000000000000 ) ) ;
#8099=CIRCLE ( 'NONE', #14544, 9.000000000000000000 ) ;
#8106=ORIENTED_EDGE ( 'NONE', *, *, #16476, .F. ) ;
#8110=CARTESIAN_POINT ( 'NONE',  ( -7.499999999999997335, -25.65291190719446490, 7.723695278929465502 ) ) ;
#8143=DIRECTION ( 'NONE',  ( -1.000000000000000000, -0.000000000000000000, -0.000000000000000000 ) ) ;
#8165=AXIS2_PLACEMENT_3D ( 'NONE', #5122, #6449, #861 ) ;
#8166=VERTEX_POINT ( 'NONE', #5835 ) ;
#8198=CARTESIAN_POINT ( 'NONE',  ( -7.499999999999996447, -23.75733333946868697, -9.035253535952438853 ) ) ;
#8216=CARTESIAN_POINT ( 'NONE',  ( 7.500000000000000888, -23.02360215807748034, 9.261711852864909389 ) ) ;
#8255=ADVANCED_FACE ( 'NONE', ( #8029 ), #12167, .F. ) ;
#8256=ORIENTED_EDGE ( 'NONE', *, *, #14132, .T. ) ;
#8282=ORIENTED_EDGE ( 'NONE', *, *, #14268, .F. ) ;
#8299=EDGE_LOOP ( 'NONE', ( #8458, #13259, #10389, #7622 ) ) ;
#8305=DIRECTION ( 'NONE',  ( 0.000000000000000000, 1.000000000000000000, 0.000000000000000000 ) ) ;
#8306=CARTESIAN_POINT ( 'NONE',  ( 7.500000000000001776, -23.02061778433118278, -9.262340467025641289 ) ) ;
#8328=FACE_OUTER_BOUND ( 'NONE', #12482, .T. ) ;
#8332=AXIS2_PLACEMENT_3D ( 'NONE', #5653, #12177, #68 ) ;
#8337=DIRECTION ( 'NONE',  ( -1.000000000000000000, -1.772429021826857464E-16, 0.000000000000000000 ) ) ;
#8344=CARTESIAN_POINT ( 'NONE',  ( 12.50000000000000000, -18.00000000000000355, 8.999999999999998224 ) ) ;
#8372=VERTEX_POINT ( 'NONE', #17378 ) ;
#8392=CARTESIAN_POINT ( 'NONE',  ( 7.500000000000004441, -25.82389322351430039, -7.532295102519075414 ) ) ;
#8458=ORIENTED_EDGE ( 'NONE', *, *, #16476, .T. ) ;
#8461=AXIS2_PLACEMENT_3D ( 'NONE', #155, #8305, #6975 ) ;
#8466=AXIS2_PLACEMENT_3D ( 'NONE', #3313, #8727, #11278 ) ;
#8481=CARTESIAN_POINT ( 'NONE',  ( 7.500000000000002665, -27.73865070282584000, -2.034160311361948636 ) ) ;
#8502=ADVANCED_FACE ( 'NONE', ( #3663 ), #4821, .T. ) ;
#8508=DIRECTION ( 'NONE',  ( 0.000000000000000000, -1.000000000000000000, 0.000000000000000000 ) ) ;
#8531=DIRECTION ( 'NONE',  ( 0.000000000000000000, 0.000000000000000000, 1.000000000000000000 ) ) ;
#8548=ORIENTED_EDGE ( 'NONE', *, *, #10569, .T. ) ;
#8567=CARTESIAN_POINT ( 'NONE',  ( 7.500000000000002665, -27.80914044117234596, 0.5315352956498873294 ) ) ;
#8575=CARTESIAN_POINT ( 'NONE',  ( 0.000000000000000000, -22.00000000000000000, 0.000000000000000000 ) ) ;
#8645=ORIENTED_EDGE ( 'NONE', *, *, #17130, .T. ) ;
#8654=CARTESIAN_POINT ( 'NONE',  ( 1.469576158976824144E-15, -22.00000000000000000, -12.00000000000000178 ) ) ;
#8727=DIRECTION ( 'NONE',  ( 1.000000000000000000, 0.000000000000000000, 0.000000000000000000 ) ) ;
#8742=EDGE_CURVE ( 'NONE', #967, #8820, #3922, .T. ) ;
#8781=VERTEX_POINT ( 'NONE', #12947 ) ;
#8820=VERTEX_POINT ( 'NONE', #16919 ) ;
#8849=ORIENTED_EDGE ( 'NONE', *, *, #2014, .F. ) ;
#8931=AXIS2_PLACEMENT_3D ( 'NONE', #13094, #2205, #15818 ) ;
#8943=CARTESIAN_POINT ( 'NONE',  ( 0.000000000000000000, 0.000000000000000000, 0.000000000000000000 ) ) ;
#8990=ORIENTED_EDGE ( 'NONE', *, *, #10879, .T. ) ;
#8998=CARTESIAN_POINT ( 'NONE',  ( 0.000000000000000000, 73.00000000000001421, 0.000000000000000000 ) ) ;
#9001=DIRECTION ( 'NONE',  ( 0.000000000000000000, -1.000000000000000000, 0.000000000000000000 ) ) ;
#9036=AXIS2_PLACEMENT_3D ( 'NONE', #5928, #6992, #5580 ) ;
#9079=ADVANCED_FACE ( 'NONE', ( #14926 ), #2730, .T. ) ;
#9084=ORIENTED_EDGE ( 'NONE', *, *, #16917, .T. ) ;
#9114=VECTOR ( 'NONE', #14236, 1000.000000000000000 ) ;
#9156=ORIENTED_EDGE ( 'NONE', *, *, #986, .T. ) ;
#9167=DIRECTION ( 'NONE',  ( -9.637352644315595243E-17, 1.000000000000000000, 0.000000000000000000 ) ) ;
#9173=ORIENTED_EDGE ( 'NONE', *, *, #11084, .F. ) ;
#9179=CARTESIAN_POINT ( 'NONE',  ( -7.499999999999999112, -24.45288220904213361, -8.693347190813744518 ) ) ;
#9244=ORIENTED_EDGE ( 'NONE', *, *, #1955, .F. ) ;
#9298=ADVANCED_FACE ( 'NONE', ( #9663 ), #3427, .T. ) ;
#9353=CARTESIAN_POINT ( 'NONE',  ( -7.499999999999995559, -27.73865070282584355, 2.034160311361949525 ) ) ;
#9392=CIRCLE ( 'NONE', #7693, 5.000000000000000000 ) ;
#9451=EDGE_LOOP ( 'NONE', ( #970, #8548 ) ) ;
#9479=ADVANCED_FACE ( 'NONE', ( #6920 ), #12297, .F. ) ;
#9527=CARTESIAN_POINT ( 'NONE',  ( -7.499999999999994671, -26.29769599445798534, -6.931232109908926020 ) ) ;
#9538=VERTEX_POINT ( 'NONE', #3041 ) ;
#9542=CARTESIAN_POINT ( 'NONE',  ( 7.500000000000003553, -22.25602869842713716, 9.367496997597598352 ) ) ;
#9598=CIRCLE ( 'NONE', #3380, 9.000000000000000000 ) ;
#9606=CARTESIAN_POINT ( 'NONE',  ( 0.000000000000000000, 3.000000000000000000, 0.000000000000000000 ) ) ;
#9628=VERTEX_POINT ( 'NONE', #10208 ) ;
#9663=FACE_OUTER_BOUND ( 'NONE', #15671, .T. ) ;
#9699=AXIS2_PLACEMENT_3D ( 'NONE', #8943, #14130, #1932 ) ;
#9746=CIRCLE ( 'NONE', #6357, 9.000000000000001776 ) ;
#9758=DIRECTION ( 'NONE',  ( 0.000000000000000000, -0.000000000000000000, -1.000000000000000000 ) ) ;
#9806=DIRECTION ( 'NONE',  ( 0.000000000000000000, -1.000000000000000000, 0.000000000000000000 ) ) ;
#9829=( LENGTH_UNIT ( ) NAMED_UNIT ( * ) SI_UNIT ( .MILLI., .METRE. ) );
#9880=EDGE_CURVE ( 'NONE', #9538, #4482, #6203, .T. ) ;
#9954=DIRECTION ( 'NONE',  ( 0.000000000000000000, 0.000000000000000000, 1.000000000000000000 ) ) ;
#9960=EDGE_LOOP ( 'NONE', ( #2912, #6404 ) ) ;
#9964=AXIS2_PLACEMENT_3D ( 'NONE', #10452, #12916, #3537 ) ;
#9999=CARTESIAN_POINT ( 'NONE',  ( 0.000000000000000000, -22.00000000000000000, 0.000000000000000000 ) ) ;
#10040=EDGE_CURVE ( 'NONE', #11330, #14612, #17194, .T. ) ;
#10070=CARTESIAN_POINT ( 'NONE',  ( 7.500000000000003553, -25.08439332921293996, -8.253836299850741298 ) ) ;
#10085=DIRECTION ( 'NONE',  ( -1.772429021826857464E-16, 1.000000000000000000, 0.000000000000000000 ) ) ;
#10093=AXIS2_PLACEMENT_3D ( 'NONE', #1018, #10492, #6428 ) ;
#10114=EDGE_CURVE ( 'NONE', #16561, #5051, #3080, .T. ) ;
#10142=CIRCLE ( 'NONE', #8461, 5.000000000000000000 ) ;
#10147=DIRECTION ( 'NONE',  ( -0.000000000000000000, -1.000000000000000000, -0.000000000000000000 ) ) ;
#10155=CARTESIAN_POINT ( 'NONE',  ( -7.499999999999996447, -22.51612366527185571, -9.346045933502390213 ) ) ;
#10198=AXIS2_PLACEMENT_3D ( 'NONE', #7048, #15314, #11017 ) ;
#10208=CARTESIAN_POINT ( 'NONE',  ( -12.50000000000000000, -22.00000000000000355, -1.714505518806294835E-15 ) ) ;
#10209=DIRECTION ( 'NONE',  ( 0.000000000000000000, 0.000000000000000000, 1.000000000000000000 ) ) ;
#10222=DIRECTION ( 'NONE',  ( -1.000000000000000000, -0.000000000000000000, -0.000000000000000000 ) ) ;
#10232=AXIS2_PLACEMENT_3D ( 'NONE', #4772, #3351, #11493 ) ;
#10309=CLOSED_SHELL ( 'NONE', ( #9079, #9479, #7916, #6652, #11622, #2652, #9298, #2266, #5808, #6046, #16371, #7438, #12090, #16671, #11862, #12950, #7137, #5708, #14210, #8502, #16138, #8255, #455, #10776 ) ) ;
#10316=EDGE_LOOP ( 'NONE', ( #7388, #4900, #1598, #11813, #17294, #8106 ) ) ;
#10389=ORIENTED_EDGE ( 'NONE', *, *, #15578, .T. ) ;
#10419=AXIS2_PLACEMENT_3D ( 'NONE', #8575, #4496, #15072 ) ;
#10422=CARTESIAN_POINT ( 'NONE',  ( 0.000000000000000000, -28.00000000000000000, 0.000000000000000000 ) ) ;
#10425=ORIENTED_EDGE ( 'NONE', *, *, #12732, .T. ) ;
#10452=CARTESIAN_POINT ( 'NONE',  ( 12.50000000000000000, -18.00000000000000355, -2.204364238465235822E-15 ) ) ;
#10492=DIRECTION ( 'NONE',  ( 1.000000000000000000, 1.301042606982605567E-16, 0.000000000000000000 ) ) ;
#10515=DIRECTION ( 'NONE',  ( -0.000000000000000000, 1.000000000000000000, -0.000000000000000000 ) ) ;
#10530=DIRECTION ( 'NONE',  ( -0.000000000000000000, -0.000000000000000000, 1.000000000000000000 ) ) ;
#10550=CARTESIAN_POINT ( 'NONE',  ( 12.50000000000000000, -18.00000000000000355, -2.204364238465235822E-15 ) ) ;
#10569=EDGE_CURVE ( 'NONE', #14419, #13897, #14918, .T. ) ;
#10622=EDGE_CURVE ( 'NONE', #6499, #13554, #9598, .T. ) ;
#10667=CARTESIAN_POINT ( 'NONE',  ( -7.499999999999997335, -24.01085892585522075, 8.949127168380917041 ) ) ;
#10776=ADVANCED_FACE ( 'NONE', ( #13619, #14935 ), #12128, .T. ) ;
#10790=CIRCLE ( 'NONE', #3164, 22.50000000000000355 ) ;
#10816=CIRCLE ( 'NONE', #15864, 6.000000000000000000 ) ;
#10834=ORIENTED_EDGE ( 'NONE', *, *, #13434, .F. ) ;
#10850=CARTESIAN_POINT ( 'NONE',  ( 12.50000000000000000, -18.00000000000000355, -2.204364238465235822E-15 ) ) ;
#10879=EDGE_CURVE ( 'NONE', #16659, #11880, #4224, .T. ) ;
#10885=CIRCLE ( 'NONE', #8931, 9.000000000000000000 ) ;
#10894=ORIENTED_EDGE ( 'NONE', *, *, #2855, .T. ) ;
#10923=ORIENTED_EDGE ( 'NONE', *, *, #7001, .T. ) ;
#10961=DIRECTION ( 'NONE',  ( 0.000000000000000000, 0.000000000000000000, -1.000000000000000000 ) ) ;
#10988=ORIENTED_EDGE ( 'NONE', *, *, #2367, .F. ) ;
#10990=CARTESIAN_POINT ( 'NONE',  ( 0.000000000000000000, 73.00000000000001421, -5.000000000000000000 ) ) ;
#10994=FACE_OUTER_BOUND ( 'NONE', #14592, .T. ) ;
#11000=FACE_BOUND ( 'NONE', #2132, .T. ) ;
#11012=EDGE_LOOP ( 'NONE', ( #1710, #10894, #15413, #13533 ) ) ;
#11017=DIRECTION ( 'NONE',  ( -1.000000000000000000, -1.445602896647338917E-16, 0.000000000000000000 ) ) ;
#11027=EDGE_LOOP ( 'NONE', ( #6664, #4301, #12651, #2959 ) ) ;
#11033=CARTESIAN_POINT ( 'NONE',  ( 7.500000000000002665, -23.27176790847081023, 9.199276322163095543 ) ) ;
#11050=CARTESIAN_POINT ( 'NONE',  ( 0.000000000000000000, 0.000000000000000000, 12.00000000000000178 ) ) ;
#11084=EDGE_CURVE ( 'NONE', #11880, #16659, #3439, .T. ) ;
#11089=PLANE ( 'NONE',  #15181 ) ;
#11103=DIRECTION ( 'NONE',  ( 0.000000000000000000, 0.000000000000000000, 1.000000000000000000 ) ) ;
#11118=CARTESIAN_POINT ( 'NONE',  ( 7.500000000000000000, -22.51433466932076755, -9.346209313438661681 ) ) ;
#11138=DIRECTION ( 'NONE',  ( -1.224646799147353207E-16, 0.000000000000000000, -1.000000000000000000 ) ) ;
#11163=EDGE_LOOP ( 'NONE', ( #7308, #16882, #15715, #9244 ) ) ;
#11188=VECTOR ( 'NONE', #10147, 1000.000000000000000 ) ;
#11208=CARTESIAN_POINT ( 'NONE',  ( 7.500000000000000888, -27.69291120311264365, -2.544524385544279177 ) ) ;
#11249=ORIENTED_EDGE ( 'NONE', *, *, #7589, .F. ) ;
#11278=DIRECTION ( 'NONE',  ( 0.000000000000000000, 0.000000000000000000, -1.000000000000000000 ) ) ;
#11319=EDGE_CURVE ( 'NONE', #8372, #14612, #15108, .T. ) ;
#11324=CARTESIAN_POINT ( 'NONE',  ( -22.50000000000000355, -22.00000000000000711, -1.714505518806294835E-15 ) ) ;
#11330=VERTEX_POINT ( 'NONE', #16540 ) ;
#11364=AXIS2_PLACEMENT_3D ( 'NONE', #12213, #5775, #5420 ) ;
#11383=CARTESIAN_POINT ( 'NONE',  ( 7.500000000000000888, -25.28130420966589753, 8.086389325435073161 ) ) ;
#11392=FACE_OUTER_BOUND ( 'NONE', #13109, .T. ) ;
#11409=CARTESIAN_POINT ( 'NONE',  ( 0.000000000000000000, 0.000000000000000000, 0.000000000000000000 ) ) ;
#11458=AXIS2_PLACEMENT_3D ( 'NONE', #2461, #6567, #7892 ) ;
#11470=CARTESIAN_POINT ( 'NONE',  ( -7.499999999999996447, -22.00000000000000000, -9.367496997597603681 ) ) ;
#11493=DIRECTION ( 'NONE',  ( 0.000000000000000000, 0.000000000000000000, 1.000000000000000000 ) ) ;
#11546=ORIENTED_EDGE ( 'NONE', *, *, #12672, .T. ) ;
#11556=CARTESIAN_POINT ( 'NONE',  ( 2.755455298081545172E-15, 0.000000000000000000, 22.50000000000000355 ) ) ;
#11589=CARTESIAN_POINT ( 'NONE',  ( -7.499999999999993783, -28.00000000000000000, 9.367496997597603681 ) ) ;
#11596=DIRECTION ( 'NONE',  ( 1.000000000000000000, 0.000000000000000000, 0.000000000000000000 ) ) ;
#11622=ADVANCED_FACE ( 'NONE', ( #12640 ), #5935, .T. ) ;
#11635=ORIENTED_EDGE ( 'NONE', *, *, #12292, .T. ) ;
#11636=LINE ( 'NONE', #16926, #11188 ) ;
#11646=VECTOR ( 'NONE', #7436, 1000.000000000000000 ) ;
#11679=EDGE_LOOP ( 'NONE', ( #16794, #5734, #5099, #9156 ) ) ;
#11688=CARTESIAN_POINT ( 'NONE',  ( 7.500000000000000888, -21.99999999999990052, -9.367496997597653419 ) ) ;
#11736=EDGE_CURVE ( 'NONE', #14868, #9538, #16048, .T. ) ;
#11763=CARTESIAN_POINT ( 'NONE',  ( 7.500000000000000000, -7.999999999999998224, -22.50000000000000355 ) ) ;
#11775=LINE ( 'NONE', #17151, #7515 ) ;
#11811=VERTEX_POINT ( 'NONE', #12003 ) ;
#11813=ORIENTED_EDGE ( 'NONE', *, *, #5035, .F. ) ;
#11862=ADVANCED_FACE ( 'NONE', ( #953 ), #2262, .T. ) ;
#11880=VERTEX_POINT ( 'NONE', #3955 ) ;
#11903=CARTESIAN_POINT ( 'NONE',  ( -7.499999999999995559, -27.73625732136943611, -2.063574628993723348 ) ) ;
#11964=ORIENTED_EDGE ( 'NONE', *, *, #1587, .T. ) ;
#11988=CARTESIAN_POINT ( 'NONE',  ( -7.499999999999993783, -27.68990399256867718, -2.572187159835569226 ) ) ;
#12003=CARTESIAN_POINT ( 'NONE',  ( 7.500000000000000888, -18.00000000000000355, 8.999999999999998224 ) ) ;
#12071=LINE ( 'NONE', #12156, #13947 ) ;
#12072=CARTESIAN_POINT ( 'NONE',  ( -7.499999999999996447, -27.80979767490545740, 0.4943161440816092322 ) ) ;
#12090=ADVANCED_FACE ( 'NONE', ( #10994 ), #549, .T. ) ;
#12121=CARTESIAN_POINT ( 'NONE',  ( 0.000000000000000000, 0.000000000000000000, 0.000000000000000000 ) ) ;
#12128=PLANE ( 'NONE',  #14089 ) ;
#12140=DIRECTION ( 'NONE',  ( 0.000000000000000000, 1.000000000000000000, 0.000000000000000000 ) ) ;
#12153=DIRECTION ( 'NONE',  ( -9.637352644315595243E-17, 1.000000000000000000, 0.000000000000000000 ) ) ;
#12156=CARTESIAN_POINT ( 'NONE',  ( 7.500000000000000000, -28.00000000000000000, 9.367496997597600128 ) ) ;
#12167=CYLINDRICAL_SURFACE ( 'NONE', #255, 4.000000000000000000 ) ;
#12177=DIRECTION ( 'NONE',  ( -1.000000000000000000, -0.000000000000000000, -0.000000000000000000 ) ) ;
#12213=CARTESIAN_POINT ( 'NONE',  ( 0.000000000000000000, -22.00000000000000000, 0.000000000000000000 ) ) ;
#12216=ORIENTED_EDGE ( 'NONE', *, *, #13084, .T. ) ;
#12230=CARTESIAN_POINT ( 'NONE',  ( 0.000000000000000000, 0.000000000000000000, 0.000000000000000000 ) ) ;
#12292=EDGE_CURVE ( 'NONE', #14612, #11330, #9392, .T. ) ;
#12297=CYLINDRICAL_SURFACE ( 'NONE', #6775, 4.000000000000000000 ) ;
#12352=CARTESIAN_POINT ( 'NONE',  ( 7.500000000000003553, -26.29769599445798534, 6.931232109908926908 ) ) ;
#12369=DIRECTION ( 'NONE',  ( 0.000000000000000000, 0.000000000000000000, -1.000000000000000000 ) ) ;
#12422=EDGE_LOOP ( 'NONE', ( #15785, #9173 ) ) ;
#12443=CARTESIAN_POINT ( 'NONE',  ( 7.500000000000001776, -27.68990399256866652, 2.572187159835578552 ) ) ;
#12476=CARTESIAN_POINT ( 'NONE',  ( 12.50000000000000000, -18.00000000000000355, -9.000000000000001776 ) ) ;
#12482=EDGE_LOOP ( 'NONE', ( #2868, #6864 ) ) ;
#12531=CARTESIAN_POINT ( 'NONE',  ( 7.500000000000000888, -27.80979767490545029, -0.4943161440816083441 ) ) ;
#12585=LINE ( 'NONE', #7285, #9114 ) ;
#12602=STYLED_ITEM('',(#17498),#3043);
#12616=CARTESIAN_POINT ( 'NONE',  ( 7.500000000000000888, -26.30006709664695563, -6.927727048493003359 ) ) ;
#12636=UNCERTAINTY_MEASURE_WITH_UNIT (LENGTH_MEASURE( 1.000000000000000082E-05 ), #9829, 'distance_accuracy_value', 'NONE');
#12640=FACE_OUTER_BOUND ( 'NONE', #757, .T. ) ;
#12651=ORIENTED_EDGE ( 'NONE', *, *, #2014, .T. ) ;
#12655=EDGE_LOOP ( 'NONE', ( #6749, #2498 ) ) ;
#12672=EDGE_CURVE ( 'NONE', #16820, #7842, #10790, .T. ) ;
#12703=CARTESIAN_POINT ( 'NONE',  ( 7.500000000000003553, -27.55009420329275471, -3.560038493048078401 ) ) ;
#12731=DIRECTION ( 'NONE',  ( 0.000000000000000000, 0.000000000000000000, 1.000000000000000000 ) ) ;
#12732=EDGE_CURVE ( 'NONE', #15368, #16820, #4774, .T. ) ;
#12769=CIRCLE ( 'NONE', #6287, 9.000000000000001776 ) ;
#12782=FACE_OUTER_BOUND ( 'NONE', #6448, .T. ) ;
#12867=VECTOR ( 'NONE', #16511, 1000.000000000000000 ) ;
#12880=( GEOMETRIC_REPRESENTATION_CONTEXT ( 3 ) GLOBAL_UNCERTAINTY_ASSIGNED_CONTEXT ( ( #12636 ) ) GLOBAL_UNIT_ASSIGNED_CONTEXT ( ( #9829, #5754, #16424 ) ) REPRESENTATION_CONTEXT ( 'NONE', 'WORKASPACE' ) );
#12916=DIRECTION ( 'NONE',  ( 1.000000000000000000, 0.000000000000000000, 0.000000000000000000 ) ) ;
#12947=CARTESIAN_POINT ( 'NONE',  ( 7.499999999999996447, -8.000000000000000000, 9.367496997597600128 ) ) ;
#12950=ADVANCED_FACE ( 'NONE', ( #4349 ), #1420, .T. ) ;
#12956=LINE ( 'NONE', #15324, #14532 ) ;
#12977=VERTEX_POINT ( 'NONE', #8344 ) ;
#12999=ORIENTED_EDGE ( 'NONE', *, *, #5035, .T. ) ;
#13005=( GEOMETRIC_REPRESENTATION_CONTEXT ( 3 ) GLOBAL_UNCERTAINTY_ASSIGNED_CONTEXT ( ( #16690 ) ) GLOBAL_UNIT_ASSIGNED_CONTEXT ( ( #13772, #15356, #868 ) ) REPRESENTATION_CONTEXT ( 'NONE', 'WORKASPACE' ) );
#13009=DIRECTION ( 'NONE',  ( 0.000000000000000000, 0.000000000000000000, -1.000000000000000000 ) ) ;
#13040=CARTESIAN_POINT ( 'NONE',  ( -7.499999999999996447, -21.99999999999990052, 9.367496997597656971 ) ) ;
#13066=AXIS2_PLACEMENT_3D ( 'NONE', #7164, #346, #12369 ) ;
#13084=EDGE_CURVE ( 'NONE', #8166, #1252, #13326, .T. ) ;
#13085=ORIENTED_EDGE ( 'NONE', *, *, #17130, .F. ) ;
#13094=CARTESIAN_POINT ( 'NONE',  ( 12.50000000000000000, -18.00000000000000355, -2.204364238465235822E-15 ) ) ;
#13105=EDGE_LOOP ( 'NONE', ( #16623, #1084, #2851, #2760 ) ) ;
#13109=EDGE_LOOP ( 'NONE', ( #13285, #2782, #992, #14782, #12999, #628 ) ) ;
#13183=CARTESIAN_POINT ( 'NONE',  ( 0.000000000000000000, 0.000000000000000000, 0.000000000000000000 ) ) ;
#13209=DIRECTION ( 'NONE',  ( -1.000000000000000000, -1.301042606982605567E-16, -0.000000000000000000 ) ) ;
#13220=CARTESIAN_POINT ( 'NONE',  ( -7.499999999999994671, -23.99662210092440517, -8.932545650451688246 ) ) ;
#13222=TOROIDAL_SURFACE ( 'NONE', #16307, 6.000000000000001776, 6.000000000000000000 ) ;
#13232=DIRECTION ( 'NONE',  ( 0.000000000000000000, 1.000000000000000000, 0.000000000000000000 ) ) ;
#13259=ORIENTED_EDGE ( 'NONE', *, *, #17449, .F. ) ;
#13280=ORIENTED_EDGE ( 'NONE', *, *, #9880, .T. ) ;
#13285=ORIENTED_EDGE ( 'NONE', *, *, #15702, .F. ) ;
#13306=CARTESIAN_POINT ( 'NONE',  ( -7.499999999999992895, -26.57032277106731755, 6.479247348114219207 ) ) ;
#13314=DIRECTION ( 'NONE',  ( 1.000000000000000000, 8.673617379884039170E-17, -0.000000000000000000 ) ) ;
#13326=CIRCLE ( 'NONE', #11364, 12.00000000000000178 ) ;
#13427=DIRECTION ( 'NONE',  ( 0.000000000000000000, 0.000000000000000000, -1.000000000000000000 ) ) ;
#13434=EDGE_CURVE ( 'NONE', #16561, #4303, #12585, .T. ) ;
#13475=CARTESIAN_POINT ( 'NONE',  ( -7.499999999999996447, -23.27176790847080667, -9.199276322163099096 ) ) ;
#13499=AXIS2_PLACEMENT_3D ( 'NONE', #15597, #9001, #6010 ) ;
#13513=PLANE ( 'NONE',  #7441 ) ;
#13533=ORIENTED_EDGE ( 'NONE', *, *, #5543, .F. ) ;
#13554=VERTEX_POINT ( 'NONE', #832 ) ;
#13562=CARTESIAN_POINT ( 'NONE',  ( -7.499999999999992895, -27.79580463407382851, -1.043242051446495733 ) ) ;
#13586=AXIS2_PLACEMENT_3D ( 'NONE', #5031, #10515, #5300 ) ;
#13610=DIRECTION ( 'NONE',  ( 0.000000000000000000, 0.000000000000000000, 1.000000000000000000 ) ) ;
#13612=FACE_OUTER_BOUND ( 'NONE', #13870, .T. ) ;
#13619=FACE_OUTER_BOUND ( 'NONE', #6249, .T. ) ;
#13658=ORIENTED_EDGE ( 'NONE', *, *, #1177, .F. ) ;
#13721=AXIS2_PLACEMENT_3D ( 'NONE', #606, #10085, #15435 ) ;
#13726=ORIENTED_EDGE ( 'NONE', *, *, #17449, .T. ) ;
#13745=CARTESIAN_POINT ( 'NONE',  ( 7.500000000000000888, -27.00941661075428613, -5.548846425319421627 ) ) ;
#13772=( LENGTH_UNIT ( ) NAMED_UNIT ( * ) SI_UNIT ( .MILLI., .METRE. ) );
#13801=AXIS2_PLACEMENT_3D ( 'NONE', #10550, #6828, #13610 ) ;
#13831=FACE_OUTER_BOUND ( 'NONE', #10316, .T. ) ;
#13848=CARTESIAN_POINT ( 'NONE',  ( 6.123233995736766282E-16, 73.00000000000001421, 5.000000000000000000 ) ) ;
#13870=EDGE_LOOP ( 'NONE', ( #5007, #6409 ) ) ;
#13875=ORIENTED_EDGE ( 'NONE', *, *, #3600, .T. ) ;
#13897=VERTEX_POINT ( 'NONE', #5352 ) ;
#13920=CARTESIAN_POINT ( 'NONE',  ( 7.500000000000001776, -23.75733333946869408, 9.035253535952435300 ) ) ;
#13945=DIRECTION ( 'NONE',  ( 1.000000000000000000, 0.000000000000000000, 0.000000000000000000 ) ) ;
#13947=VECTOR ( 'NONE', #6433, 1000.000000000000000 ) ;
#13962=ORIENTED_EDGE ( 'NONE', *, *, #17013, .T. ) ;
#13970=AXIS2_PLACEMENT_3D ( 'NONE', #1125, #7948, #6622 ) ;
#13978=CARTESIAN_POINT ( 'NONE',  ( 0.000000000000000000, -22.00000000000000000, -6.000000000000001776 ) ) ;
#13980=CARTESIAN_POINT ( 'NONE',  ( -7.499999999999998224, -8.000000000000000000, -9.367496997597607233 ) ) ;
#13992=EDGE_CURVE ( 'NONE', #7222, #11811, #12769, .T. ) ;
#14009=CARTESIAN_POINT ( 'NONE',  ( 7.500000000000004441, -25.28385182205995818, -8.084116494856626645 ) ) ;
#14089=AXIS2_PLACEMENT_3D ( 'NONE', #8081, #6838, #1601 ) ;
#14091=FACE_OUTER_BOUND ( 'NONE', #15061, .T. ) ;
#14127=FACE_OUTER_BOUND ( 'NONE', #7822, .T. ) ;
#14130=DIRECTION ( 'NONE',  ( 0.000000000000000000, 1.000000000000000000, 0.000000000000000000 ) ) ;
#14132=EDGE_CURVE ( 'NONE', #13554, #6499, #71, .T. ) ;
#14177=VECTOR ( 'NONE', #7355, 1000.000000000000000 ) ;
#14210=ADVANCED_FACE ( 'NONE', ( #13612 ), #16165, .F. ) ;
#14225=CARTESIAN_POINT ( 'NONE',  ( 12.50000000000000000, -18.00000000000000355, -2.204364238465235822E-15 ) ) ;
#14236=DIRECTION ( 'NONE',  ( -0.000000000000000000, 1.000000000000000000, -0.000000000000000000 ) ) ;
#14264=ORIENTED_EDGE ( 'NONE', *, *, #10622, .F. ) ;
#14268=EDGE_CURVE ( 'NONE', #4303, #1772, #3448, .T. ) ;
#14272=PLANE ( 'NONE',  #15876 ) ;
#14356=CARTESIAN_POINT ( 'NONE',  ( 12.50000000000000000, -14.00000000000000178, -2.204364238465235822E-15 ) ) ;
#14371=CARTESIAN_POINT ( 'NONE',  ( 7.500000000000000888, -18.00000000000000355, -2.204364238465235822E-15 ) ) ;
#14419=VERTEX_POINT ( 'NONE', #15015 ) ;
#14528=CARTESIAN_POINT ( 'NONE',  ( -7.499999999999994671, -26.30006709664694853, 6.927727048493009576 ) ) ;
#14532=VECTOR ( 'NONE', #500, 1000.000000000000000 ) ;
#14544=AXIS2_PLACEMENT_3D ( 'NONE', #3203, #15121, #7378 ) ;
#14546=EDGE_CURVE ( 'NONE', #9628, #11880, #3446, .T. ) ;
#14592=EDGE_LOOP ( 'NONE', ( #7686, #6314, #4768, #11635 ) ) ;
#14596=ORIENTED_EDGE ( 'NONE', *, *, #14132, .F. ) ;
#14612=VERTEX_POINT ( 'NONE', #4607 ) ;
#14617=CARTESIAN_POINT ( 'NONE',  ( -7.499999999999993783, -25.08364130939904157, -8.254396200996691135 ) ) ;
#14662=DIRECTION ( 'NONE',  ( -1.000000000000000000, -0.000000000000000000, -0.000000000000000000 ) ) ;
#14667=CARTESIAN_POINT ( 'NONE',  ( 0.000000000000000000, -28.00000000000000000, 12.00000000000000178 ) ) ;
#14702=EDGE_CURVE ( 'NONE', #7842, #16820, #8001, .T. ) ;
#14774=LINE ( 'NONE', #2664, #7315 ) ;
#14782=ORIENTED_EDGE ( 'NONE', *, *, #10114, .F. ) ;
#14788=CARTESIAN_POINT ( 'NONE',  ( -7.499999999999993783, -27.54571194363307995, -3.584587286925202232 ) ) ;
#14868=VERTEX_POINT ( 'NONE', #13980 ) ;
#14871=CARTESIAN_POINT ( 'NONE',  ( -7.499999999999997335, -25.28130420966591174, -8.086389325435080266 ) ) ;
#14887=CIRCLE ( 'NONE', #2200, 9.000000000000000000 ) ;
#14918=CIRCLE ( 'NONE', #7328, 6.000000000000001776 ) ;
#14926=FACE_OUTER_BOUND ( 'NONE', #11012, .T. ) ;
#14935=FACE_BOUND ( 'NONE', #12422, .T. ) ;
#14943=DIRECTION ( 'NONE',  ( 0.000000000000000000, 0.000000000000000000, -1.000000000000000000 ) ) ;
#14958=DIRECTION ( 'NONE',  ( 0.000000000000000000, 1.000000000000000000, 0.000000000000000000 ) ) ;
#15014=DIRECTION ( 'NONE',  ( 0.000000000000000000, 0.000000000000000000, -1.000000000000000000 ) ) ;
#15015=CARTESIAN_POINT ( 'NONE',  ( 1.102182119232618108E-15, -28.00000000000000000, 6.000000000000001776 ) ) ;
#15020=ORIENTED_EDGE ( 'NONE', *, *, #2426, .T. ) ;
#15022=CARTESIAN_POINT ( 'NONE',  ( 0.000000000000000000, -28.00000000000000000, 0.000000000000000000 ) ) ;
#15057=EDGE_CURVE ( 'NONE', #15368, #16449, #3745, .T. ) ;
#15061=EDGE_LOOP ( 'NONE', ( #9084, #7927, #2221, #11249 ) ) ;
#15063=DIRECTION ( 'NONE',  ( 0.000000000000000000, 0.000000000000000000, -1.000000000000000000 ) ) ;
#15072=DIRECTION ( 'NONE',  ( 1.776356839400250465E-15, 0.000000000000000000, -1.000000000000000000 ) ) ;
#15108=LINE ( 'NONE', #10990, #15277 ) ;
#15121=DIRECTION ( 'NONE',  ( 1.000000000000000000, 0.000000000000000000, 0.000000000000000000 ) ) ;
#15125=CIRCLE ( 'NONE', #13721, 12.00000000000000178 ) ;
#15154=CARTESIAN_POINT ( 'NONE',  ( 7.500000000000000888, -25.65063367634387959, 7.726132535793202472 ) ) ;
#15171=DIRECTION ( 'NONE',  ( -0.000000000000000000, 1.000000000000000000, -0.000000000000000000 ) ) ;
#15181=AXIS2_PLACEMENT_3D ( 'NONE', #12230, #12140, #5350 ) ;
#15204=DIRECTION ( 'NONE',  ( -0.000000000000000000, -1.000000000000000000, -0.000000000000000000 ) ) ;
#15237=EDGE_LOOP ( 'NONE', ( #14596, #14264 ) ) ;
#15244=CARTESIAN_POINT ( 'NONE',  ( 7.500000000000001776, -27.45244706754152020, -4.067225351102822017 ) ) ;
#15264=EDGE_CURVE ( 'NONE', #8372, #17275, #17006, .T. ) ;
#15277=VECTOR ( 'NONE', #112, 1000.000000000000000 ) ;
#15314=DIRECTION ( 'NONE',  ( -8.862145109134287319E-17, 1.000000000000000000, 0.000000000000000000 ) ) ;
#15324=CARTESIAN_POINT ( 'NONE',  ( -22.50000000000000355, -14.00000000000000533, -2.204364238465235822E-15 ) ) ;
#15328=CARTESIAN_POINT ( 'NONE',  ( 0.000000000000000000, -22.00000000000000000, 0.000000000000000000 ) ) ;
#15356=( NAMED_UNIT ( * ) PLANE_ANGLE_UNIT ( ) SI_UNIT ( $, .RADIAN. ) );
#15368=VERTEX_POINT ( 'NONE', #6148 ) ;
#15413=ORIENTED_EDGE ( 'NONE', *, *, #13992, .T. ) ;
#15421=CARTESIAN_POINT ( 'NONE',  ( 7.500000000000001776, -24.46203974633109368, -8.709571264514700317 ) ) ;
#15435=DIRECTION ( 'NONE',  ( -1.000000000000000000, -1.445602896647338917E-16, 0.000000000000000000 ) ) ;
#15519=PRODUCT_DEFINITION_FORMATION_WITH_SPECIFIED_SOURCE ( 'ANY', '', #4088, .NOT_KNOWN. ) ;
#15566=ORIENTED_EDGE ( 'NONE', *, *, #11319, .F. ) ;
#15578=EDGE_CURVE ( 'NONE', #6383, #8781, #6380, .T. ) ;
#15597=CARTESIAN_POINT ( 'NONE',  ( 0.000000000000000000, -22.00000000000000000, 0.000000000000000000 ) ) ;
#15637=DIRECTION ( 'NONE',  ( 8.673617379884037937E-17, -1.000000000000000000, 0.000000000000000000 ) ) ;
#15662=DIRECTION ( 'NONE',  ( 0.000000000000000000, 0.000000000000000000, 1.000000000000000000 ) ) ;
#15671=EDGE_LOOP ( 'NONE', ( #1603, #10425, #11546, #8849 ) ) ;
#15702=EDGE_CURVE ( 'NONE', #8166, #14419, #10816, .T. ) ;
#15715=ORIENTED_EDGE ( 'NONE', *, *, #11084, .T. ) ;
#15747=EDGE_CURVE ( 'NONE', #13897, #14419, #4028, .T. ) ;
#15772=AXIS2_PLACEMENT_3D ( 'NONE', #4254, #191, #15014 ) ;
#15785=ORIENTED_EDGE ( 'NONE', *, *, #10879, .F. ) ;
#15818=DIRECTION ( 'NONE',  ( 0.000000000000000000, 0.000000000000000000, -1.000000000000000000 ) ) ;
#15856=AXIS2_PLACEMENT_3D ( 'NONE', #6678, #13209, #9167 ) ;
#15860=CARTESIAN_POINT ( 'NONE',  ( -7.499999999999993783, -27.17584396961776250, -5.080312676971237451 ) ) ;
#15864=AXIS2_PLACEMENT_3D ( 'NONE', #2981, #4147, #11138 ) ;
#15876=AXIS2_PLACEMENT_3D ( 'NONE', #8998, #6090, #7672 ) ;
#15894=CARTESIAN_POINT ( 'NONE',  ( 12.50000000000000000, -18.00000000000000355, 8.999999999999998224 ) ) ;
#15948=B_SPLINE_CURVE_WITH_KNOTS ( 'NONE', 3,
 ( #11470, #4749, #10155, #2503, #13475, #8198, #13220, #9179, #2414, #14617, #14871, #16202, #17450, #9527, #3938, #3767, #15860, #5283, #14788, #11988, #11903, #13562, #6690, #12072, #1452, #9353, #2678, #3851, #5365, #4113, #1108, #13306, #14528, #7847, #8110, #6524, #5545, #1361, #10667, #17280, #17369, #5194, #6779, #6870 ),
 .UNSPECIFIED., .F., .F.,
 ( 4, 2, 2, 2, 2, 2, 2, 2, 2, 2, 2, 2, 2, 2, 2, 2, 2, 2, 2, 2, 2, 4 ),
 ( 0.03689401835950766734, 0.03766257893388839234, 0.03843113950826912428, 0.03919970008264984929, 0.03996826065703057429, 0.04073682123141130623, 0.04150538180579202430, 0.04304250295455348124, 0.04457962410331493125, 0.04611674525207638820, 0.04765386640083783820, 0.04919098754959928821, 0.05072810869836074515, 0.05226522984712220210, 0.05380235099588365211, 0.05533947214464510905, 0.05687659329340656600, 0.05764515386778729100, 0.05841371444216801601, 0.05995083559092945213, 0.06071939616531016326, 0.06148795673969088826 ),
 .UNSPECIFIED. ) ;
#15990=CARTESIAN_POINT ( 'NONE',  ( 7.500000000000000000, -7.999999999999998224, -22.50000000000000355 ) ) ;
#16048=LINE ( 'NONE', #6624, #5146 ) ;
#16126=ORIENTED_EDGE ( 'NONE', *, *, #986, .F. ) ;
#16138=ADVANCED_FACE ( 'NONE', ( #8328, #6646 ), #6999, .F. ) ;
#16156=FACE_BOUND ( 'NONE', #9960, .T. ) ;
#16165=PLANE ( 'NONE',  #1194 ) ;
#16202=CARTESIAN_POINT ( 'NONE',  ( -7.499999999999994671, -25.65063367634388314, -7.726132535793207801 ) ) ;
#16218=CARTESIAN_POINT ( 'NONE',  ( 0.000000000000000000, 3.000000000000000000, -22.50000000000000355 ) ) ;
#16223=VECTOR ( 'NONE', #8143, 1000.000000000000000 ) ;
#16226=APPLICATION_CONTEXT ( 'automotive_design' ) ;
#16251=VECTOR ( 'NONE', #7985, 1000.000000000000000 ) ;
#16307=AXIS2_PLACEMENT_3D ( 'NONE', #15328, #9806, #3051 ) ;
#16348=AXIS2_PLACEMENT_3D ( 'NONE', #14225, #11596, #6386 ) ;
#16371=ADVANCED_FACE ( 'NONE', ( #16156, #4065 ), #13513, .T. ) ;
#16403=CARTESIAN_POINT ( 'NONE',  ( -12.50000000000000000, -18.00000000000000355, -2.204364238465235822E-15 ) ) ;
#16424=( NAMED_UNIT ( * ) SI_UNIT ( $, .STERADIAN. ) SOLID_ANGLE_UNIT ( ) );
#16444=EDGE_LOOP ( 'NONE', ( #16487, #197 ) ) ;
#16449=VERTEX_POINT ( 'NONE', #16218 ) ;
#16470=ORIENTED_EDGE ( 'NONE', *, *, #5455, .T. ) ;
#16476=EDGE_CURVE ( 'NONE', #1252, #2386, #16803, .T. ) ;
#16487=ORIENTED_EDGE ( 'NONE', *, *, #15264, .T. ) ;
#16492=CARTESIAN_POINT ( 'NONE',  ( 7.500000000000001776, -24.66999453389980346, 8.557281619885985791 ) ) ;
#16511=DIRECTION ( 'NONE',  ( -0.000000000000000000, -1.000000000000000000, -0.000000000000000000 ) ) ;
#16540=CARTESIAN_POINT ( 'NONE',  ( 6.123233995736766282E-16, 3.000000000000000000, 5.000000000000000000 ) ) ;
#16561=VERTEX_POINT ( 'NONE', #8654 ) ;
#16582=CARTESIAN_POINT ( 'NONE',  ( 7.500000000000000000, -24.01085892585522430, -8.949127168380909936 ) ) ;
#16623=ORIENTED_EDGE ( 'NONE', *, *, #2426, .F. ) ;
#16638=VECTOR ( 'NONE', #2102, 1000.000000000000000 ) ;
#16654=AXIS2_PLACEMENT_3D ( 'NONE', #186, #4335, #13945 ) ;
#16659=VERTEX_POINT ( 'NONE', #14356 ) ;
#16669=CARTESIAN_POINT ( 'NONE',  ( 7.500000000000001776, -26.56718630404941806, 6.484415072061724850 ) ) ;
#16671=ADVANCED_FACE ( 'NONE', ( #3585 ), #14272, .T. ) ;
#16690=UNCERTAINTY_MEASURE_WITH_UNIT (LENGTH_MEASURE( 1.000000000000000082E-05 ), #13772, 'distance_accuracy_value', 'NONE');
#16755=CARTESIAN_POINT ( 'NONE',  ( 7.500000000000002665, -27.00452558693061533, 5.560661329642322848 ) ) ;
#16794=ORIENTED_EDGE ( 'NONE', *, *, #2855, .F. ) ;
#16803=B_SPLINE_CURVE_WITH_KNOTS ( 'NONE', 3,
 ( #4130, #9542, #2785, #8216, #11033, #13920, #1814, #246, #16492, #6000, #11383, #15154, #1556, #12352, #16669, #16755, #4663, #7061, #3052, #12443, #5912, #7145, #8567, #12531, #2962, #8481, #11208, #12703, #15244, #7228, #13745, #417, #12616, #8392, #5737, #14009, #10070, #15421, #16582, #4487, #8306, #11118, #4576, #4397 ),
 .UNSPECIFIED., .F., .F.,
 ( 4, 2, 2, 2, 2, 2, 2, 2, 2, 2, 2, 2, 2, 2, 2, 2, 2, 2, 2, 2, 2, 4 ),
 ( 0.03689401835950766734, 0.03766257893388839928, 0.03843113950826912428, 0.03919970008264984929, 0.03996826065703058123, 0.04073682123141131317, 0.04150538180579203817, 0.04304250295455348818, 0.04457962410331494513, 0.04611674525207639513, 0.04765386640083785208, 0.04919098754959930209, 0.05072810869836075209, 0.05226522984712220210, 0.05380235099588365211, 0.05533947214464510905, 0.05687659329340655906, 0.05764515386778727712, 0.05841371444216800213, 0.05995083559092944520, 0.06071939616531016326, 0.06148795673969088132 ),
 .UNSPECIFIED. ) ;
#16820=VERTEX_POINT ( 'NONE', #11556 ) ;
#16882=ORIENTED_EDGE ( 'NONE', *, *, #14546, .T. ) ;
#16917=EDGE_CURVE ( 'NONE', #5051, #4482, #15948, .T. ) ;
#16919=CARTESIAN_POINT ( 'NONE',  ( -12.50000000000000000, -18.00000000000000355, 8.999999999999998224 ) ) ;
#16926=CARTESIAN_POINT ( 'NONE',  ( 0.000000000000000000, 3.000000000000000000, -22.50000000000000355 ) ) ;
#16978=CARTESIAN_POINT ( 'NONE',  ( -12.50000000000000000, -14.00000000000000178, -2.204364238465235822E-15 ) ) ;
#16980=FACE_OUTER_BOUND ( 'NONE', #8299, .T. ) ;
#17006=CIRCLE ( 'NONE', #3173, 5.000000000000000000 ) ;
#17013=EDGE_CURVE ( 'NONE', #16449, #15368, #7369, .T. ) ;
#17098=CARTESIAN_POINT ( 'NONE',  ( 27.07453251570901642, -7.999999999999996447, -22.50000000000000355 ) ) ;
#17121=EDGE_LOOP ( 'NONE', ( #13658, #11964, #6968, #15566 ) ) ;
#17130=EDGE_CURVE ( 'NONE', #8781, #6383, #3681, .T. ) ;
#17151=CARTESIAN_POINT ( 'NONE',  ( 12.50000000000000000, -18.00000000000000355, -9.000000000000001776 ) ) ;
#17171=ORIENTED_EDGE ( 'NONE', *, *, #10114, .T. ) ;
#17182=DIRECTION ( 'NONE',  ( 9.637352644315592778E-17, -1.000000000000000000, 0.000000000000000000 ) ) ;
#17194=CIRCLE ( 'NONE', #9036, 5.000000000000000000 ) ;
#17205=CARTESIAN_POINT ( 'NONE',  ( -22.50000000000000355, -18.00000000000000711, -2.204364238465235822E-15 ) ) ;
#17275=VERTEX_POINT ( 'NONE', #7279 ) ;
#17280=CARTESIAN_POINT ( 'NONE',  ( -7.499999999999996447, -23.27245777243039271, 9.199283337799348814 ) ) ;
#17294=ORIENTED_EDGE ( 'NONE', *, *, #2487, .F. ) ;
#17318=VERTEX_POINT ( 'NONE', #16978 ) ;
#17369=CARTESIAN_POINT ( 'NONE',  ( -7.499999999999997335, -23.02061778433118278, 9.262340467025644841 ) ) ;
#17378=CARTESIAN_POINT ( 'NONE',  ( 0.000000000000000000, 73.00000000000001421, -5.000000000000000000 ) ) ;
#17381=ORIENTED_EDGE ( 'NONE', *, *, #3600, .F. ) ;
#17382=DIRECTION ( 'NONE',  ( 1.000000000000000000, 0.000000000000000000, 0.000000000000000000 ) ) ;
#17444=EDGE_LOOP ( 'NONE', ( #13962, #3907 ) ) ;
#17449=EDGE_CURVE ( 'NONE', #6383, #2386, #4428, .T. ) ;
#17450=CARTESIAN_POINT ( 'NONE',  ( -7.499999999999995559, -25.82163707610022740, -7.534909587719540447 ) ) ;
#17492=COLOUR_RGB('Dark Blue',0.08,0.2,0.34);
#17493=FILL_AREA_STYLE_COLOUR('',#17492);
#17494=FILL_AREA_STYLE('',(#17493));
#17495=SURFACE_STYLE_FILL_AREA(#17494);
#17496=SURFACE_SIDE_STYLE('',(#17495));
#17497=SURFACE_STYLE_USAGE(.BOTH.,#17496);
#17498=PRESENTATION_STYLE_ASSIGNMENT((#17497));
ENDSEC;
END-ISO-10303-21;
